ISO-10303-21;
HEADER;
/* Generated by software containing ST-Developer
 * from STEP Tools, Inc. (www.steptools.com) 
 */

FILE_DESCRIPTION(
/* description */ ('STEP AP214'),
/* implementation_level */ '2;1');

FILE_NAME(
/* name */ 'Oil_Bolt.step',
/* time_stamp */ '2026-10-05T13:15:56-07:00',
/* author */ (''),
/* organization */ (''),
/* preprocessor_version */ 'ST-DEVELOPER v20.2',
/* originating_system */ 'Autodesk Translation Framework v15.15.0.0',
/* authorisation */ '');

FILE_SCHEMA (('AUTOMOTIVE_DESIGN { 1 0 10303 214 3 1 1 }'));
ENDSEC;

DATA;
#10=MECHANICAL_DESIGN_GEOMETRIC_PRESENTATION_REPRESENTATION('',(#1353),#37881);
#227=TOROIDAL_SURFACE('',#11798,3.,2.);
#596=CONICAL_SURFACE('',#11795,3.47500000000001,0.785398163397447);
#1329=SHAPE_REPRESENTATION_RELATIONSHIP('SRR','None',#37962,#1341);
#1341=ADVANCED_BREP_SHAPE_REPRESENTATION('',(#1365),#37877);
#1353=STYLED_ITEM('',(#38023),#1365);
#1365=MANIFOLD_SOLID_BREP('Body1',#10827);
#1461=FACE_BOUND('',#2837,.T.);
#1535=PLANE('',#11807);
#1536=PLANE('',#11808);
#1537=PLANE('',#11809);
#2137=FACE_OUTER_BOUND('',#2830,.T.);
#2138=FACE_OUTER_BOUND('',#2831,.T.);
#2139=FACE_OUTER_BOUND('',#2832,.T.);
#2140=FACE_OUTER_BOUND('',#2833,.T.);
#2141=FACE_OUTER_BOUND('',#2834,.T.);
#2142=FACE_OUTER_BOUND('',#2835,.T.);
#2143=FACE_OUTER_BOUND('',#2836,.T.);
#2830=EDGE_LOOP('',(#9869,#9870,#9871,#9872));
#2831=EDGE_LOOP('',(#9873,#9874,#9875,#9876,#9877));
#2832=EDGE_LOOP('',(#9878,#9879,#9880,#9881,#9882));
#2833=EDGE_LOOP('',(#9883,#9884,#9885,#9886));
#2834=EDGE_LOOP('',(#9887));
#2835=EDGE_LOOP('',(#9888));
#2836=EDGE_LOOP('',(#9889));
#2837=EDGE_LOOP('',(#9890));
#3106=LINE('',#37644,#3407);
#3107=LINE('',#37657,#3408);
#3108=LINE('',#37661,#3409);
#3407=VECTOR('',#13791,3.47500000000001);
#3408=VECTOR('',#13808,5.00000000000001);
#3409=VECTOR('',#13813,3.97500000000001);
#3984=CIRCLE('',#11796,3.97500000000001);
#3985=CIRCLE('',#11797,3.47500000000001);
#3986=CIRCLE('',#11799,3.);
#3987=CIRCLE('',#11800,2.);
#3988=CIRCLE('',#11801,5.00000000000001);
#3989=CIRCLE('',#11802,5.00000000000001);
#3990=CIRCLE('',#11804,5.00000000000001);
#3991=CIRCLE('',#11806,3.97500000000001);
#5020=VERTEX_POINT('',#37641);
#5021=VERTEX_POINT('',#37643);
#5022=VERTEX_POINT('',#37647);
#5023=VERTEX_POINT('',#37649);
#5024=VERTEX_POINT('',#37651);
#5025=VERTEX_POINT('',#37655);
#5026=VERTEX_POINT('',#37659);
#6645=EDGE_CURVE('',#5020,#5020,#3984,.T.);
#6646=EDGE_CURVE('',#5020,#5021,#3106,.T.);
#6647=EDGE_CURVE('',#5021,#5021,#3985,.T.);
#6648=EDGE_CURVE('',#5022,#5022,#3986,.T.);
#6649=EDGE_CURVE('',#5022,#5023,#3987,.T.);
#6650=EDGE_CURVE('',#5024,#5023,#3988,.T.);
#6651=EDGE_CURVE('',#5023,#5024,#3989,.T.);
#6652=EDGE_CURVE('',#5025,#5025,#3990,.T.);
#6653=EDGE_CURVE('',#5025,#5024,#3107,.T.);
#6654=EDGE_CURVE('',#5026,#5026,#3991,.T.);
#6655=EDGE_CURVE('',#5026,#5020,#3108,.T.);
#9869=ORIENTED_EDGE('',*,*,#6645,.F.);
#9870=ORIENTED_EDGE('',*,*,#6646,.T.);
#9871=ORIENTED_EDGE('',*,*,#6647,.F.);
#9872=ORIENTED_EDGE('',*,*,#6646,.F.);
#9873=ORIENTED_EDGE('',*,*,#6648,.F.);
#9874=ORIENTED_EDGE('',*,*,#6649,.T.);
#9875=ORIENTED_EDGE('',*,*,#6650,.F.);
#9876=ORIENTED_EDGE('',*,*,#6651,.F.);
#9877=ORIENTED_EDGE('',*,*,#6649,.F.);
#9878=ORIENTED_EDGE('',*,*,#6652,.T.);
#9879=ORIENTED_EDGE('',*,*,#6653,.T.);
#9880=ORIENTED_EDGE('',*,*,#6650,.T.);
#9881=ORIENTED_EDGE('',*,*,#6651,.T.);
#9882=ORIENTED_EDGE('',*,*,#6653,.F.);
#9883=ORIENTED_EDGE('',*,*,#6654,.T.);
#9884=ORIENTED_EDGE('',*,*,#6655,.T.);
#9885=ORIENTED_EDGE('',*,*,#6645,.T.);
#9886=ORIENTED_EDGE('',*,*,#6655,.F.);
#9887=ORIENTED_EDGE('',*,*,#6647,.T.);
#9888=ORIENTED_EDGE('',*,*,#6648,.T.);
#9889=ORIENTED_EDGE('',*,*,#6652,.F.);
#9890=ORIENTED_EDGE('',*,*,#6654,.F.);
#10205=CYLINDRICAL_SURFACE('',#11803,5.00000000000001);
#10206=CYLINDRICAL_SURFACE('',#11805,3.97500000000001);
#10782=ADVANCED_FACE('',(#2137),#596,.T.);
#10783=ADVANCED_FACE('',(#2138),#227,.T.);
#10784=ADVANCED_FACE('',(#2139),#10205,.T.);
#10785=ADVANCED_FACE('',(#2140),#10206,.T.);
#10786=ADVANCED_FACE('',(#2141),#1535,.T.);
#10787=ADVANCED_FACE('',(#2142),#1536,.T.);
#10788=ADVANCED_FACE('',(#2143,#1461),#1537,.F.);
#10827=CLOSED_SHELL('',(#10782,#10783,#10784,#10785,#10786,#10787,#10788));
#11794=AXIS2_PLACEMENT_3D('',#37639,#13785,#13786);
#11795=AXIS2_PLACEMENT_3D('',#37640,#13787,#13788);
#11796=AXIS2_PLACEMENT_3D('',#37642,#13789,#13790);
#11797=AXIS2_PLACEMENT_3D('',#37645,#13792,#13793);
#11798=AXIS2_PLACEMENT_3D('',#37646,#13794,#13795);
#11799=AXIS2_PLACEMENT_3D('',#37648,#13796,#13797);
#11800=AXIS2_PLACEMENT_3D('',#37650,#13798,#13799);
#11801=AXIS2_PLACEMENT_3D('',#37652,#13800,#13801);
#11802=AXIS2_PLACEMENT_3D('',#37653,#13802,#13803);
#11803=AXIS2_PLACEMENT_3D('',#37654,#13804,#13805);
#11804=AXIS2_PLACEMENT_3D('',#37656,#13806,#13807);
#11805=AXIS2_PLACEMENT_3D('',#37658,#13809,#13810);
#11806=AXIS2_PLACEMENT_3D('',#37660,#13811,#13812);
#11807=AXIS2_PLACEMENT_3D('',#37662,#13814,#13815);
#11808=AXIS2_PLACEMENT_3D('',#37663,#13816,#13817);
#11809=AXIS2_PLACEMENT_3D('',#37664,#13818,#13819);
#13785=DIRECTION('axis',(0.,0.,1.));
#13786=DIRECTION('refdir',(1.,0.,0.));
#13787=DIRECTION('center_axis',(4.71519812073164E-16,9.75250265821225E-17,
-1.));
#13788=DIRECTION('ref_axis',(-1.,-1.38777878078144E-16,-4.71519812073164E-16));
#13789=DIRECTION('center_axis',(4.71519812073164E-16,9.75250265821225E-17,
-1.));
#13790=DIRECTION('ref_axis',(1.,-5.19029264012261E-15,4.71519812073163E-16));
#13791=DIRECTION('',(-0.707106781186547,-8.04957806758036E-17,0.707106781186548));
#13792=DIRECTION('center_axis',(-4.71519812073164E-16,-9.75250265821225E-17,
1.));
#13793=DIRECTION('ref_axis',(1.,1.38777878078144E-16,4.71519812073164E-16));
#13794=DIRECTION('center_axis',(4.71519812073164E-16,9.75250265821225E-17,
-1.));
#13795=DIRECTION('ref_axis',(-1.,-1.38777878078145E-16,-4.44089209850063E-16));
#13796=DIRECTION('center_axis',(4.71519812073164E-16,9.75250265821225E-17,
-1.));
#13797=DIRECTION('ref_axis',(-1.,-1.38777878078143E-16,-4.71519812073164E-16));
#13798=DIRECTION('center_axis',(1.63131981634091E-17,-1.,-9.75250265821225E-17));
#13799=DIRECTION('ref_axis',(1.,1.6313198163409E-17,4.44089209850063E-16));
#13800=DIRECTION('center_axis',(-4.71519812073164E-16,-9.75250265821225E-17,
1.));
#13801=DIRECTION('ref_axis',(-1.,6.07847105982273E-15,-4.71519812073163E-16));
#13802=DIRECTION('center_axis',(-4.71519812073164E-16,-9.75250265821225E-17,
1.));
#13803=DIRECTION('ref_axis',(-1.,6.07847105982273E-15,-4.71519812073163E-16));
#13804=DIRECTION('center_axis',(-4.71519812073164E-16,-9.75250265821225E-17,
1.));
#13805=DIRECTION('ref_axis',(1.,1.38777878078144E-16,4.71519812073164E-16));
#13806=DIRECTION('center_axis',(4.71519812073164E-16,9.75250265821225E-17,
-1.));
#13807=DIRECTION('ref_axis',(-1.,-1.38777878078144E-16,-4.71519812073164E-16));
#13808=DIRECTION('',(4.71519812073164E-16,9.75250265821225E-17,-1.));
#13809=DIRECTION('center_axis',(4.71519812073164E-16,9.75250265821225E-17,
-1.));
#13810=DIRECTION('ref_axis',(-1.,-1.38777878078144E-16,-4.71519812073164E-16));
#13811=DIRECTION('center_axis',(-4.71519812073164E-16,-9.75250265821225E-17,
1.));
#13812=DIRECTION('ref_axis',(1.,1.38777878078144E-16,4.71519812073164E-16));
#13813=DIRECTION('',(-4.71519812073164E-16,-9.75250265821225E-17,1.));
#13814=DIRECTION('center_axis',(4.71519812073163E-16,-9.75250265821224E-17,
1.));
#13815=DIRECTION('ref_axis',(1.,1.38777878078144E-16,-4.71519812073163E-16));
#13816=DIRECTION('center_axis',(-4.71519812073163E-16,9.75250265821224E-17,
-1.));
#13817=DIRECTION('ref_axis',(-1.,-1.38777878078144E-16,4.71519812073163E-16));
#13818=DIRECTION('center_axis',(-4.71519812073163E-16,9.75250265821224E-17,
-1.));
#13819=DIRECTION('ref_axis',(-1.,-1.38777878078144E-16,4.71519812073163E-16));
#37639=CARTESIAN_POINT('',(0.,0.,0.));
#37640=CARTESIAN_POINT('Origin',(0.,0.,10.));
#37641=CARTESIAN_POINT('',(3.97500000000002,1.13607475990613E-16,9.49999999999999));
#37642=CARTESIAN_POINT('Origin',(6.93889390390723E-15,-2.08166817117217E-14,
9.49999999999999));
#37643=CARTESIAN_POINT('',(3.47500000000001,5.66883636178462E-17,10.));
#37644=CARTESIAN_POINT('',(3.47500000000001,5.66883636178462E-17,10.));
#37645=CARTESIAN_POINT('Origin',(0.,0.,10.));
#37646=CARTESIAN_POINT('Origin',(1.38777878078145E-14,-1.38777878078145E-14,
-2.5));
#37647=CARTESIAN_POINT('',(3.00000000000003,-1.363379816016E-14,-4.49999999999999));
#37648=CARTESIAN_POINT('Origin',(2.77555756156289E-14,-4.16333634234434E-14,
-4.49999999999999));
#37649=CARTESIAN_POINT('',(5.00000000000002,-1.37962218169974E-14,-2.5));
#37650=CARTESIAN_POINT('Origin',(3.00000000000001,-1.38288482133242E-14,
-2.5));
#37651=CARTESIAN_POINT('',(-4.99999999999999,-4.20318857506523E-14,-2.5));
#37652=CARTESIAN_POINT('Origin',(1.38777878078145E-14,-1.38777878078145E-14,
-2.5));
#37653=CARTESIAN_POINT('Origin',(1.38777878078145E-14,-1.38777878078145E-14,
-2.5));
#37654=CARTESIAN_POINT('Origin',(2.77555756156289E-14,-4.16333634234434E-14,
-4.49999999999999));
#37655=CARTESIAN_POINT('',(-4.99999999999998,-4.33784388330273E-14,-2.22044604925031E-15));
#37656=CARTESIAN_POINT('Origin',(0.,0.,0.));
#37657=CARTESIAN_POINT('',(-4.99999999999998,-4.29395762134078E-14,-4.49999999999999));
#37658=CARTESIAN_POINT('Origin',(0.,0.,10.));
#37659=CARTESIAN_POINT('',(3.97500000000001,1.04009522852078E-15,1.11022302462516E-15));
#37660=CARTESIAN_POINT('Origin',(0.,0.,0.));
#37661=CARTESIAN_POINT('',(3.97500000000001,6.48449626995507E-17,10.));
#37662=CARTESIAN_POINT('Origin',(0.,0.,10.));
#37663=CARTESIAN_POINT('Origin',(2.77555756156289E-14,-4.16333634234434E-14,
-4.49999999999999));
#37664=CARTESIAN_POINT('Origin',(0.,0.,0.));
#37863=UNCERTAINTY_MEASURE_WITH_UNIT(LENGTH_MEASURE(0.01),#37882,
'DISTANCE_ACCURACY_VALUE',
'Maximum model space distance between geometric entities at asserted c
onnectivities');
#37867=UNCERTAINTY_MEASURE_WITH_UNIT(LENGTH_MEASURE(0.01),#37882,
'DISTANCE_ACCURACY_VALUE',
'Maximum model space distance between geometric entities at asserted c
onnectivities');
#37877=(
GEOMETRIC_REPRESENTATION_CONTEXT(3)
GLOBAL_UNCERTAINTY_ASSIGNED_CONTEXT((#37863))
GLOBAL_UNIT_ASSIGNED_CONTEXT((#37882,#37884,#37885))
REPRESENTATION_CONTEXT('','3D')
);
#37881=(
GEOMETRIC_REPRESENTATION_CONTEXT(3)
GLOBAL_UNCERTAINTY_ASSIGNED_CONTEXT((#37867))
GLOBAL_UNIT_ASSIGNED_CONTEXT((#37882,#37884,#37885))
REPRESENTATION_CONTEXT('','3D')
);
#37882=(
LENGTH_UNIT()
NAMED_UNIT(*)
SI_UNIT(.MILLI.,.METRE.)
);
#37884=(
NAMED_UNIT(*)
PLANE_ANGLE_UNIT()
SI_UNIT($,.RADIAN.)
);
#37885=(
NAMED_UNIT(*)
SI_UNIT($,.STERADIAN.)
SOLID_ANGLE_UNIT()
);
#37895=SHAPE_DEFINITION_REPRESENTATION(#37908,#37962);
#37908=PRODUCT_DEFINITION_SHAPE('',$,#37976);
#37962=SHAPE_REPRESENTATION('',(#11794),#37877);
#37966=PRODUCT_DEFINITION_CONTEXT('part definition',#38007,'design');
#37976=PRODUCT_DEFINITION('PS07','Oil_Bolt',#37989,#37966);
#37989=PRODUCT_DEFINITION_FORMATION('',$,#38018);
#38007=APPLICATION_CONTEXT(
'Core Data for Automotive Mechanical Design Process');
#38008=PRODUCT_CONTEXT('part definition',#38007,'mechanical');
#38018=PRODUCT('PS07','Oil_Bolt',$,(#38008));
#38023=PRESENTATION_STYLE_ASSIGNMENT((#38025));
#38025=SURFACE_STYLE_USAGE(.BOTH.,#38027);
#38027=SURFACE_SIDE_STYLE('',(#38029));
#38029=SURFACE_STYLE_FILL_AREA(#38031);
#38031=FILL_AREA_STYLE('Opaque(202,209,238)',(#38033));
#38033=FILL_AREA_STYLE_COLOUR('Opaque(202,209,238)',#38035);
#38035=COLOUR_RGB('Opaque(202,209,238)', 0.66274510, 0.83137255, 0.94901961);
ENDSEC;
END-ISO-10303-21;
